ISO-10303-21;
HEADER;
/* Generated by software containing ST-Developer
 * from STEP Tools, Inc. (www.steptools.com) 
 */

FILE_DESCRIPTION(
/* description */ ('Four-bar parallelogram arm'),
/* implementation_level */ '2;1');

FILE_NAME(
/* name */ 'Bearing cap (1).step',
/* time_stamp */ '2026-10-28T03:24:55-07:00',
/* author */ (''),
/* organization */ (''),
/* preprocessor_version */ 'ST-DEVELOPER v20.2',
/* originating_system */ 'Autodesk Translation Framework v15.17.0.0',
/* authorisation */ '');

FILE_SCHEMA (('AUTOMOTIVE_DESIGN { 1 0 10303 214 3 1 1 }'));
ENDSEC;

DATA;
#10=MECHANICAL_DESIGN_GEOMETRIC_PRESENTATION_REPRESENTATION('',(#642),#14512);
#542=SHAPE_REPRESENTATION_RELATIONSHIP('SRR','None',#14764,#592);
#592=ADVANCED_BREP_SHAPE_REPRESENTATION('',(#699),#14479);
#642=STYLED_ITEM('',(#15087),#699);
#699=MANIFOLD_SOLID_BREP('Body1',#7347);
#839=FACE_BOUND('',#1900,.T.);
#840=FACE_BOUND('',#1901,.T.);
#841=FACE_BOUND('',#1902,.T.);
#842=FACE_BOUND('',#1903,.T.);
#843=FACE_BOUND('',#1904,.T.);
#844=FACE_BOUND('',#1906,.T.);
#845=FACE_BOUND('',#1907,.T.);
#846=FACE_BOUND('',#1908,.T.);
#847=FACE_BOUND('',#1909,.T.);
#848=FACE_BOUND('',#1910,.T.);
#1097=PLANE('',#8299);
#1098=PLANE('',#8300);
#1369=FACE_OUTER_BOUND('',#1893,.T.);
#1370=FACE_OUTER_BOUND('',#1894,.T.);
#1371=FACE_OUTER_BOUND('',#1895,.T.);
#1372=FACE_OUTER_BOUND('',#1896,.T.);
#1373=FACE_OUTER_BOUND('',#1897,.T.);
#1374=FACE_OUTER_BOUND('',#1898,.T.);
#1375=FACE_OUTER_BOUND('',#1899,.T.);
#1376=FACE_OUTER_BOUND('',#1905,.T.);
#1893=EDGE_LOOP('',(#5682,#5683,#5684,#5685));
#1894=EDGE_LOOP('',(#5686,#5687,#5688,#5689));
#1895=EDGE_LOOP('',(#5690,#5691,#5692,#5693));
#1896=EDGE_LOOP('',(#5694,#5695,#5696,#5697));
#1897=EDGE_LOOP('',(#5698,#5699,#5700,#5701));
#1898=EDGE_LOOP('',(#5702,#5703,#5704,#5705));
#1899=EDGE_LOOP('',(#5706));
#1900=EDGE_LOOP('',(#5707));
#1901=EDGE_LOOP('',(#5708));
#1902=EDGE_LOOP('',(#5709));
#1903=EDGE_LOOP('',(#5710));
#1904=EDGE_LOOP('',(#5711));
#1905=EDGE_LOOP('',(#5712));
#1906=EDGE_LOOP('',(#5713));
#1907=EDGE_LOOP('',(#5714));
#1908=EDGE_LOOP('',(#5715));
#1909=EDGE_LOOP('',(#5716));
#1910=EDGE_LOOP('',(#5717));
#2501=LINE('',#12802,#2895);
#2502=LINE('',#12808,#2896);
#2503=LINE('',#12814,#2897);
#2504=LINE('',#12820,#2898);
#2505=LINE('',#12826,#2899);
#2506=LINE('',#12832,#2900);
#2895=VECTOR('',#9849,0.225);
#2896=VECTOR('',#9856,0.225);
#2897=VECTOR('',#9863,0.225);
#2898=VECTOR('',#9870,0.225);
#2899=VECTOR('',#9877,1.02);
#2900=VECTOR('',#9884,2.2);
#3252=CIRCLE('',#8282,0.225);
#3253=CIRCLE('',#8283,0.225);
#3254=CIRCLE('',#8285,0.225);
#3255=CIRCLE('',#8286,0.225);
#3256=CIRCLE('',#8288,0.225);
#3257=CIRCLE('',#8289,0.225);
#3258=CIRCLE('',#8291,0.225);
#3259=CIRCLE('',#8292,0.225);
#3260=CIRCLE('',#8294,1.02);
#3261=CIRCLE('',#8295,1.02);
#3262=CIRCLE('',#8297,2.2);
#3263=CIRCLE('',#8298,2.2);
#3774=VERTEX_POINT('',#12799);
#3775=VERTEX_POINT('',#12801);
#3776=VERTEX_POINT('',#12805);
#3777=VERTEX_POINT('',#12807);
#3778=VERTEX_POINT('',#12811);
#3779=VERTEX_POINT('',#12813);
#3780=VERTEX_POINT('',#12817);
#3781=VERTEX_POINT('',#12819);
#3782=VERTEX_POINT('',#12823);
#3783=VERTEX_POINT('',#12825);
#3784=VERTEX_POINT('',#12829);
#3785=VERTEX_POINT('',#12831);
#4472=EDGE_CURVE('',#3774,#3774,#3252,.T.);
#4473=EDGE_CURVE('',#3774,#3775,#2501,.T.);
#4474=EDGE_CURVE('',#3775,#3775,#3253,.T.);
#4475=EDGE_CURVE('',#3776,#3776,#3254,.T.);
#4476=EDGE_CURVE('',#3776,#3777,#2502,.T.);
#4477=EDGE_CURVE('',#3777,#3777,#3255,.T.);
#4478=EDGE_CURVE('',#3778,#3778,#3256,.T.);
#4479=EDGE_CURVE('',#3778,#3779,#2503,.T.);
#4480=EDGE_CURVE('',#3779,#3779,#3257,.T.);
#4481=EDGE_CURVE('',#3780,#3780,#3258,.T.);
#4482=EDGE_CURVE('',#3780,#3781,#2504,.T.);
#4483=EDGE_CURVE('',#3781,#3781,#3259,.T.);
#4484=EDGE_CURVE('',#3782,#3782,#3260,.T.);
#4485=EDGE_CURVE('',#3782,#3783,#2505,.T.);
#4486=EDGE_CURVE('',#3783,#3783,#3261,.T.);
#4487=EDGE_CURVE('',#3784,#3784,#3262,.T.);
#4488=EDGE_CURVE('',#3784,#3785,#2506,.T.);
#4489=EDGE_CURVE('',#3785,#3785,#3263,.T.);
#5682=ORIENTED_EDGE('',*,*,#4472,.F.);
#5683=ORIENTED_EDGE('',*,*,#4473,.T.);
#5684=ORIENTED_EDGE('',*,*,#4474,.F.);
#5685=ORIENTED_EDGE('',*,*,#4473,.F.);
#5686=ORIENTED_EDGE('',*,*,#4475,.F.);
#5687=ORIENTED_EDGE('',*,*,#4476,.T.);
#5688=ORIENTED_EDGE('',*,*,#4477,.F.);
#5689=ORIENTED_EDGE('',*,*,#4476,.F.);
#5690=ORIENTED_EDGE('',*,*,#4478,.F.);
#5691=ORIENTED_EDGE('',*,*,#4479,.T.);
#5692=ORIENTED_EDGE('',*,*,#4480,.F.);
#5693=ORIENTED_EDGE('',*,*,#4479,.F.);
#5694=ORIENTED_EDGE('',*,*,#4481,.F.);
#5695=ORIENTED_EDGE('',*,*,#4482,.T.);
#5696=ORIENTED_EDGE('',*,*,#4483,.F.);
#5697=ORIENTED_EDGE('',*,*,#4482,.F.);
#5698=ORIENTED_EDGE('',*,*,#4484,.F.);
#5699=ORIENTED_EDGE('',*,*,#4485,.T.);
#5700=ORIENTED_EDGE('',*,*,#4486,.T.);
#5701=ORIENTED_EDGE('',*,*,#4485,.F.);
#5702=ORIENTED_EDGE('',*,*,#4487,.F.);
#5703=ORIENTED_EDGE('',*,*,#4488,.T.);
#5704=ORIENTED_EDGE('',*,*,#4489,.T.);
#5705=ORIENTED_EDGE('',*,*,#4488,.F.);
#5706=ORIENTED_EDGE('',*,*,#4487,.T.);
#5707=ORIENTED_EDGE('',*,*,#4484,.T.);
#5708=ORIENTED_EDGE('',*,*,#4483,.T.);
#5709=ORIENTED_EDGE('',*,*,#4480,.T.);
#5710=ORIENTED_EDGE('',*,*,#4477,.T.);
#5711=ORIENTED_EDGE('',*,*,#4474,.T.);
#5712=ORIENTED_EDGE('',*,*,#4489,.F.);
#5713=ORIENTED_EDGE('',*,*,#4486,.F.);
#5714=ORIENTED_EDGE('',*,*,#4481,.T.);
#5715=ORIENTED_EDGE('',*,*,#4478,.T.);
#5716=ORIENTED_EDGE('',*,*,#4475,.T.);
#5717=ORIENTED_EDGE('',*,*,#4472,.T.);
#6787=CYLINDRICAL_SURFACE('',#8281,0.225);
#6788=CYLINDRICAL_SURFACE('',#8284,0.225);
#6789=CYLINDRICAL_SURFACE('',#8287,0.225);
#6790=CYLINDRICAL_SURFACE('',#8290,0.225);
#6791=CYLINDRICAL_SURFACE('',#8293,1.02);
#6792=CYLINDRICAL_SURFACE('',#8296,2.2);
#7074=ADVANCED_FACE('',(#1369),#6787,.F.);
#7075=ADVANCED_FACE('',(#1370),#6788,.F.);
#7076=ADVANCED_FACE('',(#1371),#6789,.F.);
#7077=ADVANCED_FACE('',(#1372),#6790,.F.);
#7078=ADVANCED_FACE('',(#1373),#6791,.F.);
#7079=ADVANCED_FACE('',(#1374),#6792,.T.);
#7080=ADVANCED_FACE('',(#1375,#839,#840,#841,#842,#843),#1097,.T.);
#7081=ADVANCED_FACE('',(#1376,#844,#845,#846,#847,#848),#1098,.F.);
#7347=CLOSED_SHELL('',(#7074,#7075,#7076,#7077,#7078,#7079,#7080,#7081));
#8280=AXIS2_PLACEMENT_3D('',#12797,#9843,#9844);
#8281=AXIS2_PLACEMENT_3D('',#12798,#9845,#9846);
#8282=AXIS2_PLACEMENT_3D('',#12800,#9847,#9848);
#8283=AXIS2_PLACEMENT_3D('',#12803,#9850,#9851);
#8284=AXIS2_PLACEMENT_3D('',#12804,#9852,#9853);
#8285=AXIS2_PLACEMENT_3D('',#12806,#9854,#9855);
#8286=AXIS2_PLACEMENT_3D('',#12809,#9857,#9858);
#8287=AXIS2_PLACEMENT_3D('',#12810,#9859,#9860);
#8288=AXIS2_PLACEMENT_3D('',#12812,#9861,#9862);
#8289=AXIS2_PLACEMENT_3D('',#12815,#9864,#9865);
#8290=AXIS2_PLACEMENT_3D('',#12816,#9866,#9867);
#8291=AXIS2_PLACEMENT_3D('',#12818,#9868,#9869);
#8292=AXIS2_PLACEMENT_3D('',#12821,#9871,#9872);
#8293=AXIS2_PLACEMENT_3D('',#12822,#9873,#9874);
#8294=AXIS2_PLACEMENT_3D('',#12824,#9875,#9876);
#8295=AXIS2_PLACEMENT_3D('',#12827,#9878,#9879);
#8296=AXIS2_PLACEMENT_3D('',#12828,#9880,#9881);
#8297=AXIS2_PLACEMENT_3D('',#12830,#9882,#9883);
#8298=AXIS2_PLACEMENT_3D('',#12833,#9885,#9886);
#8299=AXIS2_PLACEMENT_3D('',#12834,#9887,#9888);
#8300=AXIS2_PLACEMENT_3D('',#12835,#9889,#9890);
#9843=DIRECTION('axis',(0.,0.,1.));
#9844=DIRECTION('refdir',(1.,0.,0.));
#9845=DIRECTION('center_axis',(0.,1.,0.));
#9846=DIRECTION('ref_axis',(1.,0.,0.));
#9847=DIRECTION('center_axis',(0.,1.,0.));
#9848=DIRECTION('ref_axis',(1.,0.,0.));
#9849=DIRECTION('',(0.,1.,0.));
#9850=DIRECTION('center_axis',(0.,-1.,0.));
#9851=DIRECTION('ref_axis',(1.,0.,0.));
#9852=DIRECTION('center_axis',(0.,1.,0.));
#9853=DIRECTION('ref_axis',(1.,0.,0.));
#9854=DIRECTION('center_axis',(0.,1.,0.));
#9855=DIRECTION('ref_axis',(1.,0.,0.));
#9856=DIRECTION('',(0.,1.,0.));
#9857=DIRECTION('center_axis',(0.,-1.,0.));
#9858=DIRECTION('ref_axis',(1.,0.,0.));
#9859=DIRECTION('center_axis',(0.,1.,0.));
#9860=DIRECTION('ref_axis',(1.,0.,0.));
#9861=DIRECTION('center_axis',(0.,1.,0.));
#9862=DIRECTION('ref_axis',(1.,0.,0.));
#9863=DIRECTION('',(0.,1.,0.));
#9864=DIRECTION('center_axis',(0.,-1.,0.));
#9865=DIRECTION('ref_axis',(1.,0.,0.));
#9866=DIRECTION('center_axis',(0.,1.,0.));
#9867=DIRECTION('ref_axis',(1.,0.,0.));
#9868=DIRECTION('center_axis',(0.,1.,0.));
#9869=DIRECTION('ref_axis',(1.,0.,0.));
#9870=DIRECTION('',(0.,1.,0.));
#9871=DIRECTION('center_axis',(0.,-1.,0.));
#9872=DIRECTION('ref_axis',(1.,0.,0.));
#9873=DIRECTION('center_axis',(0.,1.,0.));
#9874=DIRECTION('ref_axis',(1.,0.,0.));
#9875=DIRECTION('center_axis',(0.,-1.,0.));
#9876=DIRECTION('ref_axis',(1.,0.,0.));
#9877=DIRECTION('',(0.,-1.,0.));
#9878=DIRECTION('center_axis',(0.,-1.,0.));
#9879=DIRECTION('ref_axis',(1.,0.,0.));
#9880=DIRECTION('center_axis',(0.,1.,0.));
#9881=DIRECTION('ref_axis',(1.,0.,0.));
#9882=DIRECTION('center_axis',(0.,1.,0.));
#9883=DIRECTION('ref_axis',(1.,0.,0.));
#9884=DIRECTION('',(0.,-1.,0.));
#9885=DIRECTION('center_axis',(0.,1.,0.));
#9886=DIRECTION('ref_axis',(1.,0.,0.));
#9887=DIRECTION('center_axis',(0.,1.,0.));
#9888=DIRECTION('ref_axis',(1.,0.,0.));
#9889=DIRECTION('center_axis',(0.,1.,0.));
#9890=DIRECTION('ref_axis',(1.,0.,0.));
#12797=CARTESIAN_POINT('',(0.,0.,0.));
#12798=CARTESIAN_POINT('Origin',(-1.23743686707646,0.95,6.76256313292354));
#12799=CARTESIAN_POINT('',(-1.46243686707646,1.05,6.76256313292354));
#12800=CARTESIAN_POINT('Origin',(-1.23743686707646,1.05,6.76256313292354));
#12801=CARTESIAN_POINT('',(-1.46243686707646,1.4,6.76256313292354));
#12802=CARTESIAN_POINT('',(-1.46243686707646,0.95,6.76256313292354));
#12803=CARTESIAN_POINT('Origin',(-1.23743686707646,1.4,6.76256313292354));
#12804=CARTESIAN_POINT('Origin',(-1.23743686707646,0.95,9.23743686707646));
#12805=CARTESIAN_POINT('',(-1.46243686707646,1.05,9.23743686707646));
#12806=CARTESIAN_POINT('Origin',(-1.23743686707646,1.05,9.23743686707646));
#12807=CARTESIAN_POINT('',(-1.46243686707646,1.4,9.23743686707646));
#12808=CARTESIAN_POINT('',(-1.46243686707646,0.95,9.23743686707646));
#12809=CARTESIAN_POINT('Origin',(-1.23743686707646,1.4,9.23743686707646));
#12810=CARTESIAN_POINT('Origin',(1.23743686707646,0.95,9.23743686707646));
#12811=CARTESIAN_POINT('',(1.01243686707646,1.05,9.23743686707646));
#12812=CARTESIAN_POINT('Origin',(1.23743686707646,1.05,9.23743686707646));
#12813=CARTESIAN_POINT('',(1.01243686707646,1.4,9.23743686707646));
#12814=CARTESIAN_POINT('',(1.01243686707646,0.95,9.23743686707646));
#12815=CARTESIAN_POINT('Origin',(1.23743686707646,1.4,9.23743686707646));
#12816=CARTESIAN_POINT('Origin',(1.23743686707646,0.95,6.76256313292354));
#12817=CARTESIAN_POINT('',(1.01243686707646,1.05,6.76256313292354));
#12818=CARTESIAN_POINT('Origin',(1.23743686707646,1.05,6.76256313292354));
#12819=CARTESIAN_POINT('',(1.01243686707646,1.4,6.76256313292354));
#12820=CARTESIAN_POINT('',(1.01243686707646,0.95,6.76256313292354));
#12821=CARTESIAN_POINT('Origin',(1.23743686707646,1.4,6.76256313292354));
#12822=CARTESIAN_POINT('Origin',(0.,1.05,8.));
#12823=CARTESIAN_POINT('',(-1.02,1.4,8.));
#12824=CARTESIAN_POINT('Origin',(0.,1.4,8.));
#12825=CARTESIAN_POINT('',(-1.02,1.05,8.));
#12826=CARTESIAN_POINT('',(-1.02,1.05,8.));
#12827=CARTESIAN_POINT('Origin',(0.,1.05,8.));
#12828=CARTESIAN_POINT('Origin',(0.,1.05,8.));
#12829=CARTESIAN_POINT('',(-2.2,1.4,8.));
#12830=CARTESIAN_POINT('Origin',(0.,1.4,8.));
#12831=CARTESIAN_POINT('',(-2.2,1.05,8.));
#12832=CARTESIAN_POINT('',(-2.2,1.05,8.));
#12833=CARTESIAN_POINT('Origin',(0.,1.05,8.));
#12834=CARTESIAN_POINT('Origin',(0.,1.4,8.));
#12835=CARTESIAN_POINT('Origin',(0.,1.05,8.));
#14422=UNCERTAINTY_MEASURE_WITH_UNIT(LENGTH_MEASURE(0.001),#14513,
'DISTANCE_ACCURACY_VALUE',
'Maximum model space distance between geometric entities at asserted c
onnectivities');
#14455=UNCERTAINTY_MEASURE_WITH_UNIT(LENGTH_MEASURE(0.001),#14513,
'DISTANCE_ACCURACY_VALUE',
'Maximum model space distance between geometric entities at asserted c
onnectivities');
#14479=(
GEOMETRIC_REPRESENTATION_CONTEXT(3)
GLOBAL_UNCERTAINTY_ASSIGNED_CONTEXT((#14422))
GLOBAL_UNIT_ASSIGNED_CONTEXT((#14513,#14515,#14516))
REPRESENTATION_CONTEXT('','3D')
);
#14512=(
GEOMETRIC_REPRESENTATION_CONTEXT(3)
GLOBAL_UNCERTAINTY_ASSIGNED_CONTEXT((#14455))
GLOBAL_UNIT_ASSIGNED_CONTEXT((#14513,#14515,#14516))
REPRESENTATION_CONTEXT('','3D')
);
#14513=(
LENGTH_UNIT()
NAMED_UNIT(*)
SI_UNIT(.CENTI.,.METRE.)
);
#14515=(
NAMED_UNIT(*)
PLANE_ANGLE_UNIT()
SI_UNIT($,.RADIAN.)
);
#14516=(
NAMED_UNIT(*)
SI_UNIT($,.STERADIAN.)
SOLID_ANGLE_UNIT()
);
#14540=SHAPE_DEFINITION_REPRESENTATION(#14596,#14764);
#14596=PRODUCT_DEFINITION_SHAPE('',$,#14821);
#14764=SHAPE_REPRESENTATION('',(#8280),#14479);
#14797=PRODUCT_DEFINITION_CONTEXT('part definition',#14967,'design');
#14821=PRODUCT_DEFINITION('Bearing cap (1)','Bearing cap (1)',#14877,#14797);
#14877=PRODUCT_DEFINITION_FORMATION('',$,#14992);
#14967=APPLICATION_CONTEXT(
'Core Data for Automotive Mechanical Design Process');
#14968=PRODUCT_CONTEXT('part definition',#14967,'mechanical');
#14992=PRODUCT('Bearing cap (1)','Bearing cap (1)','Bearing cap (1)',(#14968));
#15081=COLOUR_RGB('Grey',0.48,0.52,0.57);
#15082=FILL_AREA_STYLE_COLOUR('',#15081);
#15083=FILL_AREA_STYLE('',(#15082));
#15084=SURFACE_STYLE_FILL_AREA(#15083);
#15085=SURFACE_SIDE_STYLE('',(#15084));
#15086=SURFACE_STYLE_USAGE(.BOTH.,#15085);
#15087=PRESENTATION_STYLE_ASSIGNMENT((#15086));
ENDSEC;
END-ISO-10303-21;
